ISO-10303-21;
HEADER;
/* Generated by software containing ST-Developer
 * from STEP Tools, Inc. (www.steptools.com) 
 */

FILE_DESCRIPTION(
/* description */ ('Gravity roller conveyor section'),
/* implementation_level */ '2;1');

FILE_NAME(
/* name */ 'Axle support (1).step',
/* time_stamp */ '2026-11-02T07:43:02-08:00',
/* author */ (''),
/* organization */ (''),
/* preprocessor_version */ 'ST-DEVELOPER v20.2',
/* originating_system */ 'Autodesk Translation Framework v15.17.0.0',
/* authorisation */ '');

FILE_SCHEMA (('AUTOMOTIVE_DESIGN { 1 0 10303 214 3 1 1 }'));
ENDSEC;

DATA;
#10=MECHANICAL_DESIGN_GEOMETRIC_PRESENTATION_REPRESENTATION('',(#570),#13821);
#494=SHAPE_REPRESENTATION_RELATIONSHIP('SRR','None',#14033,#528);
#528=ADVANCED_BREP_SHAPE_REPRESENTATION('',(#608),#13820);
#570=STYLED_ITEM('',(#14192),#608);
#608=MANIFOLD_SOLID_BREP('Body1',#7672);
#694=FACE_BOUND('',#1919,.T.);
#695=FACE_BOUND('',#1922,.T.);
#696=FACE_BOUND('',#1927,.T.);
#697=FACE_BOUND('',#1930,.T.);
#698=FACE_BOUND('',#1933,.T.);
#699=FACE_BOUND('',#1934,.T.);
#700=FACE_BOUND('',#1936,.T.);
#701=FACE_BOUND('',#1937,.T.);
#999=PLANE('',#8764);
#1000=PLANE('',#8769);
#1001=PLANE('',#8778);
#1002=PLANE('',#8779);
#1003=PLANE('',#8780);
#1004=PLANE('',#8781);
#1005=PLANE('',#8782);
#1006=PLANE('',#8783);
#1413=FACE_OUTER_BOUND('',#1917,.T.);
#1414=FACE_OUTER_BOUND('',#1918,.T.);
#1415=FACE_OUTER_BOUND('',#1920,.T.);
#1416=FACE_OUTER_BOUND('',#1921,.T.);
#1417=FACE_OUTER_BOUND('',#1923,.T.);
#1418=FACE_OUTER_BOUND('',#1924,.T.);
#1419=FACE_OUTER_BOUND('',#1925,.T.);
#1420=FACE_OUTER_BOUND('',#1926,.T.);
#1421=FACE_OUTER_BOUND('',#1928,.T.);
#1422=FACE_OUTER_BOUND('',#1929,.T.);
#1423=FACE_OUTER_BOUND('',#1931,.T.);
#1424=FACE_OUTER_BOUND('',#1932,.T.);
#1425=FACE_OUTER_BOUND('',#1935,.T.);
#1917=EDGE_LOOP('',(#7076,#7077,#7078,#7079));
#1918=EDGE_LOOP('',(#7080));
#1919=EDGE_LOOP('',(#7081));
#1920=EDGE_LOOP('',(#7082,#7083,#7084,#7085));
#1921=EDGE_LOOP('',(#7086));
#1922=EDGE_LOOP('',(#7087));
#1923=EDGE_LOOP('',(#7088,#7089,#7090,#7091));
#1924=EDGE_LOOP('',(#7092,#7093,#7094,#7095));
#1925=EDGE_LOOP('',(#7096,#7097,#7098,#7099));
#1926=EDGE_LOOP('',(#7100,#7101,#7102,#7103));
#1927=EDGE_LOOP('',(#7104));
#1928=EDGE_LOOP('',(#7105,#7106,#7107,#7108));
#1929=EDGE_LOOP('',(#7109,#7110,#7111,#7112));
#1930=EDGE_LOOP('',(#7113));
#1931=EDGE_LOOP('',(#7114,#7115,#7116,#7117));
#1932=EDGE_LOOP('',(#7118,#7119,#7120,#7121));
#1933=EDGE_LOOP('',(#7122));
#1934=EDGE_LOOP('',(#7123));
#1935=EDGE_LOOP('',(#7124,#7125,#7126,#7127));
#1936=EDGE_LOOP('',(#7128));
#1937=EDGE_LOOP('',(#7129));
#2639=LINE('',#13657,#3357);
#2640=LINE('',#13666,#3358);
#2641=LINE('',#13674,#3359);
#2642=LINE('',#13678,#3360);
#2643=LINE('',#13683,#3361);
#2644=LINE('',#13688,#3362);
#2645=LINE('',#13690,#3363);
#2646=LINE('',#13692,#3364);
#2647=LINE('',#13693,#3365);
#2648=LINE('',#13696,#3366);
#2649=LINE('',#13698,#3367);
#2650=LINE('',#13699,#3368);
#2651=LINE('',#13702,#3369);
#2652=LINE('',#13704,#3370);
#2653=LINE('',#13705,#3371);
#2654=LINE('',#13707,#3372);
#2655=LINE('',#13708,#3373);
#3357=VECTOR('',#10948,0.5);
#3358=VECTOR('',#10959,0.5);
#3359=VECTOR('',#10970,0.275);
#3360=VECTOR('',#10975,0.275);
#3361=VECTOR('',#10980,0.505);
#3362=VECTOR('',#10985,1.);
#3363=VECTOR('',#10986,1.);
#3364=VECTOR('',#10987,1.);
#3365=VECTOR('',#10988,1.);
#3366=VECTOR('',#10991,1.);
#3367=VECTOR('',#10992,1.);
#3368=VECTOR('',#10993,1.);
#3369=VECTOR('',#10996,1.);
#3370=VECTOR('',#10997,1.);
#3371=VECTOR('',#10998,1.);
#3372=VECTOR('',#11001,1.);
#3373=VECTOR('',#11002,1.);
#3580=CIRCLE('',#8762,0.5);
#3581=CIRCLE('',#8763,0.5);
#3582=CIRCLE('',#8765,0.275);
#3583=CIRCLE('',#8767,0.5);
#3584=CIRCLE('',#8768,0.5);
#3585=CIRCLE('',#8770,0.275);
#3586=CIRCLE('',#8772,0.275);
#3587=CIRCLE('',#8774,0.275);
#3588=CIRCLE('',#8776,0.505);
#3589=CIRCLE('',#8777,0.505);
#4220=VERTEX_POINT('',#13654);
#4221=VERTEX_POINT('',#13656);
#4222=VERTEX_POINT('',#13660);
#4223=VERTEX_POINT('',#13663);
#4224=VERTEX_POINT('',#13665);
#4225=VERTEX_POINT('',#13669);
#4226=VERTEX_POINT('',#13672);
#4227=VERTEX_POINT('',#13676);
#4228=VERTEX_POINT('',#13680);
#4229=VERTEX_POINT('',#13682);
#4230=VERTEX_POINT('',#13686);
#4231=VERTEX_POINT('',#13687);
#4232=VERTEX_POINT('',#13689);
#4233=VERTEX_POINT('',#13691);
#4234=VERTEX_POINT('',#13695);
#4235=VERTEX_POINT('',#13697);
#4236=VERTEX_POINT('',#13701);
#4237=VERTEX_POINT('',#13703);
#5175=EDGE_CURVE('',#4220,#4220,#3580,.T.);
#5176=EDGE_CURVE('',#4220,#4221,#2639,.T.);
#5177=EDGE_CURVE('',#4221,#4221,#3581,.T.);
#5178=EDGE_CURVE('',#4222,#4222,#3582,.T.);
#5179=EDGE_CURVE('',#4223,#4223,#3583,.T.);
#5180=EDGE_CURVE('',#4223,#4224,#2640,.T.);
#5181=EDGE_CURVE('',#4224,#4224,#3584,.T.);
#5182=EDGE_CURVE('',#4225,#4225,#3585,.T.);
#5183=EDGE_CURVE('',#4226,#4226,#3586,.T.);
#5184=EDGE_CURVE('',#4226,#4222,#2641,.T.);
#5185=EDGE_CURVE('',#4227,#4227,#3587,.T.);
#5186=EDGE_CURVE('',#4227,#4225,#2642,.T.);
#5187=EDGE_CURVE('',#4228,#4228,#3588,.T.);
#5188=EDGE_CURVE('',#4228,#4229,#2643,.T.);
#5189=EDGE_CURVE('',#4229,#4229,#3589,.T.);
#5190=EDGE_CURVE('',#4230,#4231,#2644,.T.);
#5191=EDGE_CURVE('',#4231,#4232,#2645,.T.);
#5192=EDGE_CURVE('',#4233,#4232,#2646,.T.);
#5193=EDGE_CURVE('',#4230,#4233,#2647,.T.);
#5194=EDGE_CURVE('',#4234,#4230,#2648,.T.);
#5195=EDGE_CURVE('',#4235,#4233,#2649,.T.);
#5196=EDGE_CURVE('',#4234,#4235,#2650,.T.);
#5197=EDGE_CURVE('',#4236,#4234,#2651,.T.);
#5198=EDGE_CURVE('',#4237,#4235,#2652,.T.);
#5199=EDGE_CURVE('',#4236,#4237,#2653,.T.);
#5200=EDGE_CURVE('',#4231,#4236,#2654,.T.);
#5201=EDGE_CURVE('',#4232,#4237,#2655,.T.);
#7076=ORIENTED_EDGE('',*,*,#5175,.F.);
#7077=ORIENTED_EDGE('',*,*,#5176,.T.);
#7078=ORIENTED_EDGE('',*,*,#5177,.F.);
#7079=ORIENTED_EDGE('',*,*,#5176,.F.);
#7080=ORIENTED_EDGE('',*,*,#5175,.T.);
#7081=ORIENTED_EDGE('',*,*,#5178,.F.);
#7082=ORIENTED_EDGE('',*,*,#5179,.F.);
#7083=ORIENTED_EDGE('',*,*,#5180,.T.);
#7084=ORIENTED_EDGE('',*,*,#5181,.F.);
#7085=ORIENTED_EDGE('',*,*,#5180,.F.);
#7086=ORIENTED_EDGE('',*,*,#5179,.T.);
#7087=ORIENTED_EDGE('',*,*,#5182,.F.);
#7088=ORIENTED_EDGE('',*,*,#5183,.F.);
#7089=ORIENTED_EDGE('',*,*,#5184,.T.);
#7090=ORIENTED_EDGE('',*,*,#5178,.T.);
#7091=ORIENTED_EDGE('',*,*,#5184,.F.);
#7092=ORIENTED_EDGE('',*,*,#5185,.F.);
#7093=ORIENTED_EDGE('',*,*,#5186,.T.);
#7094=ORIENTED_EDGE('',*,*,#5182,.T.);
#7095=ORIENTED_EDGE('',*,*,#5186,.F.);
#7096=ORIENTED_EDGE('',*,*,#5187,.F.);
#7097=ORIENTED_EDGE('',*,*,#5188,.T.);
#7098=ORIENTED_EDGE('',*,*,#5189,.F.);
#7099=ORIENTED_EDGE('',*,*,#5188,.F.);
#7100=ORIENTED_EDGE('',*,*,#5190,.T.);
#7101=ORIENTED_EDGE('',*,*,#5191,.T.);
#7102=ORIENTED_EDGE('',*,*,#5192,.F.);
#7103=ORIENTED_EDGE('',*,*,#5193,.F.);
#7104=ORIENTED_EDGE('',*,*,#5189,.T.);
#7105=ORIENTED_EDGE('',*,*,#5194,.T.);
#7106=ORIENTED_EDGE('',*,*,#5193,.T.);
#7107=ORIENTED_EDGE('',*,*,#5195,.F.);
#7108=ORIENTED_EDGE('',*,*,#5196,.F.);
#7109=ORIENTED_EDGE('',*,*,#5197,.T.);
#7110=ORIENTED_EDGE('',*,*,#5196,.T.);
#7111=ORIENTED_EDGE('',*,*,#5198,.F.);
#7112=ORIENTED_EDGE('',*,*,#5199,.F.);
#7113=ORIENTED_EDGE('',*,*,#5187,.T.);
#7114=ORIENTED_EDGE('',*,*,#5200,.T.);
#7115=ORIENTED_EDGE('',*,*,#5199,.T.);
#7116=ORIENTED_EDGE('',*,*,#5201,.F.);
#7117=ORIENTED_EDGE('',*,*,#5191,.F.);
#7118=ORIENTED_EDGE('',*,*,#5201,.T.);
#7119=ORIENTED_EDGE('',*,*,#5198,.T.);
#7120=ORIENTED_EDGE('',*,*,#5195,.T.);
#7121=ORIENTED_EDGE('',*,*,#5192,.T.);
#7122=ORIENTED_EDGE('',*,*,#5177,.T.);
#7123=ORIENTED_EDGE('',*,*,#5181,.T.);
#7124=ORIENTED_EDGE('',*,*,#5200,.F.);
#7125=ORIENTED_EDGE('',*,*,#5190,.F.);
#7126=ORIENTED_EDGE('',*,*,#5194,.F.);
#7127=ORIENTED_EDGE('',*,*,#5197,.F.);
#7128=ORIENTED_EDGE('',*,*,#5183,.T.);
#7129=ORIENTED_EDGE('',*,*,#5185,.T.);
#7203=CYLINDRICAL_SURFACE('',#8761,0.5);
#7204=CYLINDRICAL_SURFACE('',#8766,0.5);
#7205=CYLINDRICAL_SURFACE('',#8771,0.275);
#7206=CYLINDRICAL_SURFACE('',#8773,0.275);
#7207=CYLINDRICAL_SURFACE('',#8775,0.505);
#7614=ADVANCED_FACE('',(#1413),#7203,.F.);
#7615=ADVANCED_FACE('',(#1414,#694),#999,.T.);
#7616=ADVANCED_FACE('',(#1415),#7204,.F.);
#7617=ADVANCED_FACE('',(#1416,#695),#1000,.T.);
#7618=ADVANCED_FACE('',(#1417),#7205,.F.);
#7619=ADVANCED_FACE('',(#1418),#7206,.F.);
#7620=ADVANCED_FACE('',(#1419),#7207,.F.);
#7621=ADVANCED_FACE('',(#1420,#696),#1001,.T.);
#7622=ADVANCED_FACE('',(#1421),#1002,.T.);
#7623=ADVANCED_FACE('',(#1422,#697),#1003,.T.);
#7624=ADVANCED_FACE('',(#1423),#1004,.T.);
#7625=ADVANCED_FACE('',(#1424,#698,#699),#1005,.T.);
#7626=ADVANCED_FACE('',(#1425,#700,#701),#1006,.F.);
#7672=CLOSED_SHELL('',(#7614,#7615,#7616,#7617,#7618,#7619,#7620,#7621,
#7622,#7623,#7624,#7625,#7626));
#8760=AXIS2_PLACEMENT_3D('',#13652,#10942,#10943);
#8761=AXIS2_PLACEMENT_3D('',#13653,#10944,#10945);
#8762=AXIS2_PLACEMENT_3D('',#13655,#10946,#10947);
#8763=AXIS2_PLACEMENT_3D('',#13658,#10949,#10950);
#8764=AXIS2_PLACEMENT_3D('',#13659,#10951,#10952);
#8765=AXIS2_PLACEMENT_3D('',#13661,#10953,#10954);
#8766=AXIS2_PLACEMENT_3D('',#13662,#10955,#10956);
#8767=AXIS2_PLACEMENT_3D('',#13664,#10957,#10958);
#8768=AXIS2_PLACEMENT_3D('',#13667,#10960,#10961);
#8769=AXIS2_PLACEMENT_3D('',#13668,#10962,#10963);
#8770=AXIS2_PLACEMENT_3D('',#13670,#10964,#10965);
#8771=AXIS2_PLACEMENT_3D('',#13671,#10966,#10967);
#8772=AXIS2_PLACEMENT_3D('',#13673,#10968,#10969);
#8773=AXIS2_PLACEMENT_3D('',#13675,#10971,#10972);
#8774=AXIS2_PLACEMENT_3D('',#13677,#10973,#10974);
#8775=AXIS2_PLACEMENT_3D('',#13679,#10976,#10977);
#8776=AXIS2_PLACEMENT_3D('',#13681,#10978,#10979);
#8777=AXIS2_PLACEMENT_3D('',#13684,#10981,#10982);
#8778=AXIS2_PLACEMENT_3D('',#13685,#10983,#10984);
#8779=AXIS2_PLACEMENT_3D('',#13694,#10989,#10990);
#8780=AXIS2_PLACEMENT_3D('',#13700,#10994,#10995);
#8781=AXIS2_PLACEMENT_3D('',#13706,#10999,#11000);
#8782=AXIS2_PLACEMENT_3D('',#13709,#11003,#11004);
#8783=AXIS2_PLACEMENT_3D('',#13710,#11005,#11006);
#10942=DIRECTION('axis',(0.,0.,1.));
#10943=DIRECTION('refdir',(1.,0.,0.));
#10944=DIRECTION('center_axis',(0.,0.,1.));
#10945=DIRECTION('ref_axis',(1.,0.,0.));
#10946=DIRECTION('center_axis',(0.,0.,1.));
#10947=DIRECTION('ref_axis',(1.,0.,0.));
#10948=DIRECTION('',(0.,0.,1.));
#10949=DIRECTION('center_axis',(0.,0.,-1.));
#10950=DIRECTION('ref_axis',(1.,0.,0.));
#10951=DIRECTION('center_axis',(0.,0.,1.));
#10952=DIRECTION('ref_axis',(1.,0.,0.));
#10953=DIRECTION('center_axis',(0.,0.,1.));
#10954=DIRECTION('ref_axis',(1.,0.,0.));
#10955=DIRECTION('center_axis',(0.,0.,1.));
#10956=DIRECTION('ref_axis',(1.,0.,0.));
#10957=DIRECTION('center_axis',(0.,0.,1.));
#10958=DIRECTION('ref_axis',(1.,0.,0.));
#10959=DIRECTION('',(0.,0.,1.));
#10960=DIRECTION('center_axis',(0.,0.,-1.));
#10961=DIRECTION('ref_axis',(1.,0.,0.));
#10962=DIRECTION('center_axis',(0.,0.,1.));
#10963=DIRECTION('ref_axis',(1.,0.,0.));
#10964=DIRECTION('center_axis',(0.,0.,1.));
#10965=DIRECTION('ref_axis',(1.,0.,0.));
#10966=DIRECTION('center_axis',(0.,0.,1.));
#10967=DIRECTION('ref_axis',(1.,0.,0.));
#10968=DIRECTION('center_axis',(0.,0.,1.));
#10969=DIRECTION('ref_axis',(1.,0.,0.));
#10970=DIRECTION('',(0.,0.,1.));
#10971=DIRECTION('center_axis',(0.,0.,1.));
#10972=DIRECTION('ref_axis',(1.,0.,0.));
#10973=DIRECTION('center_axis',(0.,0.,1.));
#10974=DIRECTION('ref_axis',(1.,0.,0.));
#10975=DIRECTION('',(0.,0.,1.));
#10976=DIRECTION('center_axis',(0.,1.,0.));
#10977=DIRECTION('ref_axis',(1.,0.,0.));
#10978=DIRECTION('center_axis',(0.,1.,0.));
#10979=DIRECTION('ref_axis',(1.,0.,0.));
#10980=DIRECTION('',(0.,1.,0.));
#10981=DIRECTION('center_axis',(0.,-1.,0.));
#10982=DIRECTION('ref_axis',(1.,0.,0.));
#10983=DIRECTION('center_axis',(0.,1.,0.));
#10984=DIRECTION('ref_axis',(-1.,0.,0.));
#10985=DIRECTION('',(-1.,0.,0.));
#10986=DIRECTION('',(0.,0.,1.));
#10987=DIRECTION('',(-1.,0.,0.));
#10988=DIRECTION('',(0.,0.,1.));
#10989=DIRECTION('center_axis',(1.,0.,0.));
#10990=DIRECTION('ref_axis',(0.,1.,0.));
#10991=DIRECTION('',(0.,1.,0.));
#10992=DIRECTION('',(0.,1.,0.));
#10993=DIRECTION('',(0.,0.,1.));
#10994=DIRECTION('center_axis',(0.,-1.,0.));
#10995=DIRECTION('ref_axis',(1.,0.,0.));
#10996=DIRECTION('',(1.,0.,0.));
#10997=DIRECTION('',(1.,0.,0.));
#10998=DIRECTION('',(0.,0.,1.));
#10999=DIRECTION('center_axis',(-1.,0.,0.));
#11000=DIRECTION('ref_axis',(0.,-1.,0.));
#11001=DIRECTION('',(0.,-1.,0.));
#11002=DIRECTION('',(0.,-1.,0.));
#11003=DIRECTION('center_axis',(0.,0.,1.));
#11004=DIRECTION('ref_axis',(1.,0.,0.));
#11005=DIRECTION('center_axis',(0.,0.,1.));
#11006=DIRECTION('ref_axis',(1.,0.,0.));
#13652=CARTESIAN_POINT('',(0.,0.,0.));
#13653=CARTESIAN_POINT('Origin',(1.6,32.,6.9));
#13654=CARTESIAN_POINT('',(1.1,32.,6.9));
#13655=CARTESIAN_POINT('Origin',(1.6,32.,6.9));
#13656=CARTESIAN_POINT('',(1.1,32.,9.));
#13657=CARTESIAN_POINT('',(1.1,32.,6.9));
#13658=CARTESIAN_POINT('Origin',(1.6,32.,9.));
#13659=CARTESIAN_POINT('Origin',(1.6,32.,6.9));
#13660=CARTESIAN_POINT('',(1.325,32.,6.9));
#13661=CARTESIAN_POINT('Origin',(1.6,32.,6.9));
#13662=CARTESIAN_POINT('Origin',(4.4,32.,6.9));
#13663=CARTESIAN_POINT('',(3.9,32.,6.9));
#13664=CARTESIAN_POINT('Origin',(4.4,32.,6.9));
#13665=CARTESIAN_POINT('',(3.9,32.,9.));
#13666=CARTESIAN_POINT('',(3.9,32.,6.9));
#13667=CARTESIAN_POINT('Origin',(4.4,32.,9.));
#13668=CARTESIAN_POINT('Origin',(4.4,32.,6.9));
#13669=CARTESIAN_POINT('',(4.125,32.,6.9));
#13670=CARTESIAN_POINT('Origin',(4.4,32.,6.9));
#13671=CARTESIAN_POINT('Origin',(1.6,32.,5.9));
#13672=CARTESIAN_POINT('',(1.325,32.,6.));
#13673=CARTESIAN_POINT('Origin',(1.6,32.,6.));
#13674=CARTESIAN_POINT('',(1.325,32.,5.9));
#13675=CARTESIAN_POINT('Origin',(4.4,32.,5.9));
#13676=CARTESIAN_POINT('',(4.125,32.,6.));
#13677=CARTESIAN_POINT('Origin',(4.4,32.,6.));
#13678=CARTESIAN_POINT('',(4.125,32.,5.9));
#13679=CARTESIAN_POINT('Origin',(3.,30.9,8.));
#13680=CARTESIAN_POINT('',(2.495,31.,8.));
#13681=CARTESIAN_POINT('Origin',(3.,31.,8.));
#13682=CARTESIAN_POINT('',(2.495,33.,8.));
#13683=CARTESIAN_POINT('',(2.495,30.9,8.));
#13684=CARTESIAN_POINT('Origin',(3.,33.,8.));
#13685=CARTESIAN_POINT('Origin',(5.,33.,6.));
#13686=CARTESIAN_POINT('',(5.,33.,6.));
#13687=CARTESIAN_POINT('',(1.,33.,6.));
#13688=CARTESIAN_POINT('',(5.,33.,6.));
#13689=CARTESIAN_POINT('',(1.,33.,9.));
#13690=CARTESIAN_POINT('',(1.,33.,6.));
#13691=CARTESIAN_POINT('',(5.,33.,9.));
#13692=CARTESIAN_POINT('',(5.,33.,9.));
#13693=CARTESIAN_POINT('',(5.,33.,6.));
#13694=CARTESIAN_POINT('Origin',(5.,31.,6.));
#13695=CARTESIAN_POINT('',(5.,31.,6.));
#13696=CARTESIAN_POINT('',(5.,31.,6.));
#13697=CARTESIAN_POINT('',(5.,31.,9.));
#13698=CARTESIAN_POINT('',(5.,31.,9.));
#13699=CARTESIAN_POINT('',(5.,31.,6.));
#13700=CARTESIAN_POINT('Origin',(1.,31.,6.));
#13701=CARTESIAN_POINT('',(1.,31.,6.));
#13702=CARTESIAN_POINT('',(1.,31.,6.));
#13703=CARTESIAN_POINT('',(1.,31.,9.));
#13704=CARTESIAN_POINT('',(1.,31.,9.));
#13705=CARTESIAN_POINT('',(1.,31.,6.));
#13706=CARTESIAN_POINT('Origin',(1.,33.,6.));
#13707=CARTESIAN_POINT('',(1.,33.,6.));
#13708=CARTESIAN_POINT('',(1.,33.,9.));
#13709=CARTESIAN_POINT('Origin',(3.,32.,9.));
#13710=CARTESIAN_POINT('Origin',(3.,32.,6.));
#13781=UNCERTAINTY_MEASURE_WITH_UNIT(LENGTH_MEASURE(0.001),#13822,
'DISTANCE_ACCURACY_VALUE',
'Maximum model space distance between geometric entities at asserted c
onnectivities');
#13782=UNCERTAINTY_MEASURE_WITH_UNIT(LENGTH_MEASURE(0.001),#13822,
'DISTANCE_ACCURACY_VALUE',
'Maximum model space distance between geometric entities at asserted c
onnectivities');
#13820=(
GEOMETRIC_REPRESENTATION_CONTEXT(3)
GLOBAL_UNCERTAINTY_ASSIGNED_CONTEXT((#13781))
GLOBAL_UNIT_ASSIGNED_CONTEXT((#13822,#13824,#13825))
REPRESENTATION_CONTEXT('','3D')
);
#13821=(
GEOMETRIC_REPRESENTATION_CONTEXT(3)
GLOBAL_UNCERTAINTY_ASSIGNED_CONTEXT((#13782))
GLOBAL_UNIT_ASSIGNED_CONTEXT((#13822,#13824,#13825))
REPRESENTATION_CONTEXT('','3D')
);
#13822=(
LENGTH_UNIT()
NAMED_UNIT(*)
SI_UNIT(.CENTI.,.METRE.)
);
#13824=(
NAMED_UNIT(*)
PLANE_ANGLE_UNIT()
SI_UNIT($,.RADIAN.)
);
#13825=(
NAMED_UNIT(*)
SI_UNIT($,.STERADIAN.)
SOLID_ANGLE_UNIT()
);
#13863=SHAPE_DEFINITION_REPRESENTATION(#13962,#14033);
#13962=PRODUCT_DEFINITION_SHAPE('',$,#14072);
#14033=SHAPE_REPRESENTATION('',(#8760),#13820);
#14034=PRODUCT_DEFINITION_CONTEXT('part definition',#14150,'design');
#14072=PRODUCT_DEFINITION('Axle support_1','Axle support (1)',#14110,#14034);
#14110=PRODUCT_DEFINITION_FORMATION('',$,#14189);
#14150=APPLICATION_CONTEXT(
'Core Data for Automotive Mechanical Design Process');
#14151=PRODUCT_CONTEXT('part definition',#14150,'mechanical');
#14189=PRODUCT('Axle support_1','Axle support (1)','Axle support',(#14151));
#14192=PRESENTATION_STYLE_ASSIGNMENT((#14197));
#14197=SURFACE_STYLE_USAGE(.BOTH.,#14202);
#14202=SURFACE_SIDE_STYLE('',(#14207));
#14207=SURFACE_STYLE_FILL_AREA(#14212);
#14212=FILL_AREA_STYLE('CAD Library Painted - Engineering blue',(#14217));
#14217=FILL_AREA_STYLE_COLOUR('CAD Library Painted - Engineering blue',
#14222);
#14222=COLOUR_RGB('CAD Library Painted - Engineering blue',0.12156862745098,
0.356862745098039,0.6);
ENDSEC;
END-ISO-10303-21;
